ISO-10303-21;
HEADER;
/* Generated by software containing ST-Developer
 * from STEP Tools, Inc. (www.steptools.com) 
 */

FILE_DESCRIPTION(
/* description */ ('Turntable on roller ring'),
/* implementation_level */ '2;1');

FILE_NAME(
/* name */ 'Axle keeper (3).step',
/* time_stamp */ '2026-10-28T03:23:59-07:00',
/* author */ (''),
/* organization */ (''),
/* preprocessor_version */ 'ST-DEVELOPER v20.2',
/* originating_system */ 'Autodesk Translation Framework v15.17.0.0',
/* authorisation */ '');

FILE_SCHEMA (('AUTOMOTIVE_DESIGN { 1 0 10303 214 3 1 1 }'));
ENDSEC;

DATA;
#10=MECHANICAL_DESIGN_GEOMETRIC_PRESENTATION_REPRESENTATION('',(#661),#16281);
#542=SHAPE_REPRESENTATION_RELATIONSHIP('SRR','None',#16562,#597);
#597=ADVANCED_BREP_SHAPE_REPRESENTATION('',(#731),#16256);
#661=STYLED_ITEM('',(#16932),#731);
#731=MANIFOLD_SOLID_BREP('Body1',#8404);
#953=FACE_BOUND('',#2324,.T.);
#954=FACE_BOUND('',#2326,.T.);
#1185=PLANE('',#9838);
#1186=PLANE('',#9839);
#1620=FACE_OUTER_BOUND('',#2321,.T.);
#1621=FACE_OUTER_BOUND('',#2322,.T.);
#1622=FACE_OUTER_BOUND('',#2323,.T.);
#1623=FACE_OUTER_BOUND('',#2325,.T.);
#2321=EDGE_LOOP('',(#7181,#7182,#7183,#7184));
#2322=EDGE_LOOP('',(#7185,#7186,#7187,#7188));
#2323=EDGE_LOOP('',(#7189));
#2324=EDGE_LOOP('',(#7190));
#2325=EDGE_LOOP('',(#7191));
#2326=EDGE_LOOP('',(#7192));
#2888=LINE('',#15166,#3371);
#2889=LINE('',#15172,#3372);
#3371=VECTOR('',#12183,0.225);
#3372=VECTOR('',#12190,0.8);
#3811=CIRCLE('',#9833,0.225);
#3812=CIRCLE('',#9834,0.225);
#3813=CIRCLE('',#9836,0.8);
#3814=CIRCLE('',#9837,0.8);
#4463=VERTEX_POINT('',#15163);
#4464=VERTEX_POINT('',#15165);
#4465=VERTEX_POINT('',#15169);
#4466=VERTEX_POINT('',#15171);
#5401=EDGE_CURVE('',#4463,#4463,#3811,.T.);
#5402=EDGE_CURVE('',#4463,#4464,#2888,.T.);
#5403=EDGE_CURVE('',#4464,#4464,#3812,.T.);
#5404=EDGE_CURVE('',#4465,#4465,#3813,.T.);
#5405=EDGE_CURVE('',#4465,#4466,#2889,.T.);
#5406=EDGE_CURVE('',#4466,#4466,#3814,.T.);
#7181=ORIENTED_EDGE('',*,*,#5401,.F.);
#7182=ORIENTED_EDGE('',*,*,#5402,.T.);
#7183=ORIENTED_EDGE('',*,*,#5403,.T.);
#7184=ORIENTED_EDGE('',*,*,#5402,.F.);
#7185=ORIENTED_EDGE('',*,*,#5404,.F.);
#7186=ORIENTED_EDGE('',*,*,#5405,.T.);
#7187=ORIENTED_EDGE('',*,*,#5406,.T.);
#7188=ORIENTED_EDGE('',*,*,#5405,.F.);
#7189=ORIENTED_EDGE('',*,*,#5404,.T.);
#7190=ORIENTED_EDGE('',*,*,#5401,.T.);
#7191=ORIENTED_EDGE('',*,*,#5406,.F.);
#7192=ORIENTED_EDGE('',*,*,#5403,.F.);
#7811=CYLINDRICAL_SURFACE('',#9832,0.225);
#7812=CYLINDRICAL_SURFACE('',#9835,0.8);
#8223=ADVANCED_FACE('',(#1620),#7811,.F.);
#8224=ADVANCED_FACE('',(#1621),#7812,.T.);
#8225=ADVANCED_FACE('',(#1622,#953),#1185,.T.);
#8226=ADVANCED_FACE('',(#1623,#954),#1186,.F.);
#8404=CLOSED_SHELL('',(#8223,#8224,#8225,#8226));
#9831=AXIS2_PLACEMENT_3D('',#15161,#12177,#12178);
#9832=AXIS2_PLACEMENT_3D('',#15162,#12179,#12180);
#9833=AXIS2_PLACEMENT_3D('',#15164,#12181,#12182);
#9834=AXIS2_PLACEMENT_3D('',#15167,#12184,#12185);
#9835=AXIS2_PLACEMENT_3D('',#15168,#12186,#12187);
#9836=AXIS2_PLACEMENT_3D('',#15170,#12188,#12189);
#9837=AXIS2_PLACEMENT_3D('',#15173,#12191,#12192);
#9838=AXIS2_PLACEMENT_3D('',#15174,#12193,#12194);
#9839=AXIS2_PLACEMENT_3D('',#15175,#12195,#12196);
#12177=DIRECTION('axis',(0.,0.,1.));
#12178=DIRECTION('refdir',(1.,0.,0.));
#12179=DIRECTION('center_axis',(0.,1.,0.));
#12180=DIRECTION('ref_axis',(1.,0.,0.));
#12181=DIRECTION('center_axis',(0.,-1.,0.));
#12182=DIRECTION('ref_axis',(1.,0.,0.));
#12183=DIRECTION('',(0.,-1.,0.));
#12184=DIRECTION('center_axis',(0.,-1.,0.));
#12185=DIRECTION('ref_axis',(1.,0.,0.));
#12186=DIRECTION('center_axis',(0.,1.,0.));
#12187=DIRECTION('ref_axis',(1.,0.,0.));
#12188=DIRECTION('center_axis',(0.,1.,0.));
#12189=DIRECTION('ref_axis',(1.,0.,0.));
#12190=DIRECTION('',(0.,-1.,0.));
#12191=DIRECTION('center_axis',(0.,1.,0.));
#12192=DIRECTION('ref_axis',(1.,0.,0.));
#12193=DIRECTION('center_axis',(0.,1.,0.));
#12194=DIRECTION('ref_axis',(1.,0.,0.));
#12195=DIRECTION('center_axis',(0.,1.,0.));
#12196=DIRECTION('ref_axis',(1.,0.,0.));
#15161=CARTESIAN_POINT('',(0.,0.,0.));
#15162=CARTESIAN_POINT('Origin',(0.,16.3,3.5));
#15163=CARTESIAN_POINT('',(-0.225,16.5,3.5));
#15164=CARTESIAN_POINT('Origin',(0.,16.5,3.5));
#15165=CARTESIAN_POINT('',(-0.225,16.3,3.5));
#15166=CARTESIAN_POINT('',(-0.225,16.3,3.5));
#15167=CARTESIAN_POINT('Origin',(0.,16.3,3.5));
#15168=CARTESIAN_POINT('Origin',(0.,16.3,3.5));
#15169=CARTESIAN_POINT('',(-0.8,16.5,3.5));
#15170=CARTESIAN_POINT('Origin',(0.,16.5,3.5));
#15171=CARTESIAN_POINT('',(-0.8,16.3,3.5));
#15172=CARTESIAN_POINT('',(-0.8,16.3,3.5));
#15173=CARTESIAN_POINT('Origin',(0.,16.3,3.5));
#15174=CARTESIAN_POINT('Origin',(0.,16.5,3.5));
#15175=CARTESIAN_POINT('Origin',(0.,16.3,3.5));
#16187=UNCERTAINTY_MEASURE_WITH_UNIT(LENGTH_MEASURE(0.001),#16282,
'DISTANCE_ACCURACY_VALUE',
'Maximum model space distance between geometric entities at asserted c
onnectivities');
#16212=UNCERTAINTY_MEASURE_WITH_UNIT(LENGTH_MEASURE(0.001),#16282,
'DISTANCE_ACCURACY_VALUE',
'Maximum model space distance between geometric entities at asserted c
onnectivities');
#16256=(
GEOMETRIC_REPRESENTATION_CONTEXT(3)
GLOBAL_UNCERTAINTY_ASSIGNED_CONTEXT((#16187))
GLOBAL_UNIT_ASSIGNED_CONTEXT((#16282,#16284,#16285))
REPRESENTATION_CONTEXT('','3D')
);
#16281=(
GEOMETRIC_REPRESENTATION_CONTEXT(3)
GLOBAL_UNCERTAINTY_ASSIGNED_CONTEXT((#16212))
GLOBAL_UNIT_ASSIGNED_CONTEXT((#16282,#16284,#16285))
REPRESENTATION_CONTEXT('','3D')
);
#16282=(
LENGTH_UNIT()
NAMED_UNIT(*)
SI_UNIT(.CENTI.,.METRE.)
);
#16284=(
NAMED_UNIT(*)
PLANE_ANGLE_UNIT()
SI_UNIT($,.RADIAN.)
);
#16285=(
NAMED_UNIT(*)
SI_UNIT($,.STERADIAN.)
SOLID_ANGLE_UNIT()
);
#16329=SHAPE_DEFINITION_REPRESENTATION(#16423,#16562);
#16423=PRODUCT_DEFINITION_SHAPE('',$,#16631);
#16562=SHAPE_REPRESENTATION('',(#9831),#16256);
#16587=PRODUCT_DEFINITION_CONTEXT('part definition',#16793,'design');
#16631=PRODUCT_DEFINITION('Axle keeper (3)','Axle keeper (3)',#16699,#16587);
#16699=PRODUCT_DEFINITION_FORMATION('',$,#16838);
#16793=APPLICATION_CONTEXT(
'Core Data for Automotive Mechanical Design Process');
#16794=PRODUCT_CONTEXT('part definition',#16793,'mechanical');
#16838=PRODUCT('Axle keeper (3)','Axle keeper (3)','Axle keeper (3)',(#16794));
#16926=COLOUR_RGB('Grey',0.48,0.52,0.57);
#16927=FILL_AREA_STYLE_COLOUR('',#16926);
#16928=FILL_AREA_STYLE('',(#16927));
#16929=SURFACE_STYLE_FILL_AREA(#16928);
#16930=SURFACE_SIDE_STYLE('',(#16929));
#16931=SURFACE_STYLE_USAGE(.BOTH.,#16930);
#16932=PRESENTATION_STYLE_ASSIGNMENT((#16931));
ENDSEC;
END-ISO-10303-21;
